ISO-10303-21;
HEADER;
/* Generated by software containing ST-Developer
 * from STEP Tools, Inc. (www.steptools.com) 
 */

FILE_DESCRIPTION(
/* description */ ('PAT-041'),
/* implementation_level */ '2;1');

FILE_NAME(
/* name */ 'Flat Washer - M8.step',
/* time_stamp */ '2026-10-28T22:21:24-07:00',
/* author */ (''),
/* organization */ (''),
/* preprocessor_version */ 'ST-DEVELOPER v20.2',
/* originating_system */ 'Autodesk Translation Framework v15.17.0.0',
/* authorisation */ '');

FILE_SCHEMA (('AUTOMOTIVE_DESIGN { 1 0 10303 214 3 1 1 }'));
ENDSEC;

DATA;
#10=MECHANICAL_DESIGN_GEOMETRIC_PRESENTATION_REPRESENTATION('',(#217),#2507);
#197=SHAPE_REPRESENTATION_RELATIONSHIP('SRR','None',#2582,#207);
#207=ADVANCED_BREP_SHAPE_REPRESENTATION('',(#227),#2505);
#217=STYLED_ITEM('',(#2701),#227);
#227=MANIFOLD_SOLID_BREP('Body1',#1337);
#276=FACE_BOUND('',#490,.T.);
#277=FACE_BOUND('',#492,.T.);
#303=PLANE('',#1586);
#304=PLANE('',#1587);
#369=FACE_OUTER_BOUND('',#487,.T.);
#370=FACE_OUTER_BOUND('',#488,.T.);
#371=FACE_OUTER_BOUND('',#489,.T.);
#372=FACE_OUTER_BOUND('',#491,.T.);
#487=EDGE_LOOP('',(#1162,#1163,#1164,#1165));
#488=EDGE_LOOP('',(#1166,#1167,#1168,#1169));
#489=EDGE_LOOP('',(#1170));
#490=EDGE_LOOP('',(#1171));
#491=EDGE_LOOP('',(#1172));
#492=EDGE_LOOP('',(#1173));
#551=LINE('',#2358,#607);
#552=LINE('',#2364,#608);
#607=VECTOR('',#1952,0.42);
#608=VECTOR('',#1959,0.8);
#682=CIRCLE('',#1581,0.42);
#683=CIRCLE('',#1582,0.42);
#684=CIRCLE('',#1584,0.8);
#685=CIRCLE('',#1585,0.8);
#766=VERTEX_POINT('',#2355);
#767=VERTEX_POINT('',#2357);
#768=VERTEX_POINT('',#2361);
#769=VERTEX_POINT('',#2363);
#901=EDGE_CURVE('',#766,#766,#682,.T.);
#902=EDGE_CURVE('',#766,#767,#551,.T.);
#903=EDGE_CURVE('',#767,#767,#683,.T.);
#904=EDGE_CURVE('',#768,#768,#684,.T.);
#905=EDGE_CURVE('',#768,#769,#552,.T.);
#906=EDGE_CURVE('',#769,#769,#685,.T.);
#1162=ORIENTED_EDGE('',*,*,#901,.F.);
#1163=ORIENTED_EDGE('',*,*,#902,.T.);
#1164=ORIENTED_EDGE('',*,*,#903,.T.);
#1165=ORIENTED_EDGE('',*,*,#902,.F.);
#1166=ORIENTED_EDGE('',*,*,#904,.F.);
#1167=ORIENTED_EDGE('',*,*,#905,.T.);
#1168=ORIENTED_EDGE('',*,*,#906,.T.);
#1169=ORIENTED_EDGE('',*,*,#905,.F.);
#1170=ORIENTED_EDGE('',*,*,#904,.T.);
#1171=ORIENTED_EDGE('',*,*,#901,.T.);
#1172=ORIENTED_EDGE('',*,*,#906,.F.);
#1173=ORIENTED_EDGE('',*,*,#903,.F.);
#1255=CYLINDRICAL_SURFACE('',#1580,0.42);
#1256=CYLINDRICAL_SURFACE('',#1583,0.8);
#1314=ADVANCED_FACE('',(#369),#1255,.F.);
#1315=ADVANCED_FACE('',(#370),#1256,.T.);
#1316=ADVANCED_FACE('',(#371,#276),#303,.T.);
#1317=ADVANCED_FACE('',(#372,#277),#304,.F.);
#1337=CLOSED_SHELL('',(#1314,#1315,#1316,#1317));
#1579=AXIS2_PLACEMENT_3D('',#2353,#1946,#1947);
#1580=AXIS2_PLACEMENT_3D('',#2354,#1948,#1949);
#1581=AXIS2_PLACEMENT_3D('',#2356,#1950,#1951);
#1582=AXIS2_PLACEMENT_3D('',#2359,#1953,#1954);
#1583=AXIS2_PLACEMENT_3D('',#2360,#1955,#1956);
#1584=AXIS2_PLACEMENT_3D('',#2362,#1957,#1958);
#1585=AXIS2_PLACEMENT_3D('',#2365,#1960,#1961);
#1586=AXIS2_PLACEMENT_3D('',#2366,#1962,#1963);
#1587=AXIS2_PLACEMENT_3D('',#2367,#1964,#1965);
#1946=DIRECTION('axis',(0.,0.,1.));
#1947=DIRECTION('refdir',(1.,0.,0.));
#1948=DIRECTION('center_axis',(0.,1.,0.));
#1949=DIRECTION('ref_axis',(1.,0.,0.));
#1950=DIRECTION('center_axis',(0.,-1.,0.));
#1951=DIRECTION('ref_axis',(1.,0.,0.));
#1952=DIRECTION('',(0.,-1.,0.));
#1953=DIRECTION('center_axis',(0.,-1.,0.));
#1954=DIRECTION('ref_axis',(1.,0.,0.));
#1955=DIRECTION('center_axis',(0.,1.,0.));
#1956=DIRECTION('ref_axis',(1.,0.,0.));
#1957=DIRECTION('center_axis',(0.,1.,0.));
#1958=DIRECTION('ref_axis',(1.,0.,0.));
#1959=DIRECTION('',(0.,-1.,0.));
#1960=DIRECTION('center_axis',(0.,1.,0.));
#1961=DIRECTION('ref_axis',(1.,0.,0.));
#1962=DIRECTION('center_axis',(0.,1.,0.));
#1963=DIRECTION('ref_axis',(1.,0.,0.));
#1964=DIRECTION('center_axis',(0.,1.,0.));
#1965=DIRECTION('ref_axis',(1.,0.,0.));
#2353=CARTESIAN_POINT('',(0.,0.,0.));
#2354=CARTESIAN_POINT('Origin',(0.,0.,0.));
#2355=CARTESIAN_POINT('',(-0.42,0.16,5.14351655641888E-17));
#2356=CARTESIAN_POINT('Origin',(0.,0.16,0.));
#2357=CARTESIAN_POINT('',(-0.42,0.,5.14351655641888E-17));
#2358=CARTESIAN_POINT('',(-0.42,0.,5.14351655641888E-17));
#2359=CARTESIAN_POINT('Origin',(0.,0.,0.));
#2360=CARTESIAN_POINT('Origin',(0.,0.,0.));
#2361=CARTESIAN_POINT('',(-0.8,0.16,9.79717439317883E-17));
#2362=CARTESIAN_POINT('Origin',(0.,0.16,0.));
#2363=CARTESIAN_POINT('',(-0.8,0.,9.79717439317883E-17));
#2364=CARTESIAN_POINT('',(-0.8,0.,9.79717439317883E-17));
#2365=CARTESIAN_POINT('Origin',(0.,0.,0.));
#2366=CARTESIAN_POINT('Origin',(0.,0.16,0.));
#2367=CARTESIAN_POINT('Origin',(0.,0.,0.));
#2493=UNCERTAINTY_MEASURE_WITH_UNIT(LENGTH_MEASURE(0.001),#2508,
'DISTANCE_ACCURACY_VALUE',
'Maximum model space distance between geometric entities at asserted c
onnectivities');
#2495=UNCERTAINTY_MEASURE_WITH_UNIT(LENGTH_MEASURE(0.001),#2508,
'DISTANCE_ACCURACY_VALUE',
'Maximum model space distance between geometric entities at asserted c
onnectivities');
#2505=(
GEOMETRIC_REPRESENTATION_CONTEXT(3)
GLOBAL_UNCERTAINTY_ASSIGNED_CONTEXT((#2493))
GLOBAL_UNIT_ASSIGNED_CONTEXT((#2508,#2510,#2511))
REPRESENTATION_CONTEXT('','3D')
);
#2507=(
GEOMETRIC_REPRESENTATION_CONTEXT(3)
GLOBAL_UNCERTAINTY_ASSIGNED_CONTEXT((#2495))
GLOBAL_UNIT_ASSIGNED_CONTEXT((#2508,#2510,#2511))
REPRESENTATION_CONTEXT('','3D')
);
#2508=(
LENGTH_UNIT()
NAMED_UNIT(*)
SI_UNIT(.CENTI.,.METRE.)
);
#2510=(
NAMED_UNIT(*)
PLANE_ANGLE_UNIT()
SI_UNIT($,.RADIAN.)
);
#2511=(
NAMED_UNIT(*)
SI_UNIT($,.STERADIAN.)
SOLID_ANGLE_UNIT()
);
#2521=SHAPE_DEFINITION_REPRESENTATION(#2532,#2582);
#2532=PRODUCT_DEFINITION_SHAPE('',$,#2594);
#2582=SHAPE_REPRESENTATION('',(#1579),#2505);
#2584=PRODUCT_DEFINITION_CONTEXT('part definition',#2619,'design');
#2594=PRODUCT_DEFINITION('Flat Washer - M8','Flat Washer - M8',
#2605,#2584);
#2605=PRODUCT_DEFINITION_FORMATION('',$,#2630);
#2619=APPLICATION_CONTEXT(
'Core Data for Automotive Mechanical Design Process');
#2620=PRODUCT_CONTEXT('part definition',#2619,'mechanical');
#2630=PRODUCT('Flat Washer - M8','Flat Washer - M8',
'Flat Washer - M8',(#2620));
#2695=COLOUR_RGB('Black',0.12,0.14,0.17);
#2696=FILL_AREA_STYLE_COLOUR('',#2695);
#2697=FILL_AREA_STYLE('',(#2696));
#2698=SURFACE_STYLE_FILL_AREA(#2697);
#2699=SURFACE_SIDE_STYLE('',(#2698));
#2700=SURFACE_STYLE_USAGE(.BOTH.,#2699);
#2701=PRESENTATION_STYLE_ASSIGNMENT((#2700));
ENDSEC;
END-ISO-10303-21;
